ISO-10303-21;
HEADER;
/* Generated by software containing ST-Developer
 * from STEP Tools, Inc. (www.steptools.com) 
 */

FILE_DESCRIPTION(
/* description */ ('Cam-driven reciprocating slide'),
/* implementation_level */ '2;1');

FILE_NAME(
/* name */ 'Camshaft bearing post (1).step',
/* time_stamp */ '2026-10-28T03:25:20-07:00',
/* author */ (''),
/* organization */ (''),
/* preprocessor_version */ 'ST-DEVELOPER v20.2',
/* originating_system */ 'Autodesk Translation Framework v15.17.0.0',
/* authorisation */ '');

FILE_SCHEMA (('AUTOMOTIVE_DESIGN { 1 0 10303 214 3 1 1 }'));
ENDSEC;

DATA;
#10=MECHANICAL_DESIGN_GEOMETRIC_PRESENTATION_REPRESENTATION('',(#428),#13277);
#354=SHAPE_REPRESENTATION_RELATIONSHIP('SRR','None',#13447,#391);
#391=ADVANCED_BREP_SHAPE_REPRESENTATION('',(#472),#13242);
#428=STYLED_ITEM('',(#13720),#472);
#472=MANIFOLD_SOLID_BREP('Body1',#6404);
#556=FACE_BOUND('',#1403,.T.);
#557=FACE_BOUND('',#1405,.T.);
#558=FACE_BOUND('',#1409,.T.);
#559=FACE_BOUND('',#1410,.T.);
#560=FACE_BOUND('',#1411,.T.);
#561=FACE_BOUND('',#1412,.T.);
#562=FACE_BOUND('',#1413,.T.);
#563=FACE_BOUND('',#1416,.T.);
#564=FACE_BOUND('',#1417,.T.);
#565=FACE_BOUND('',#1418,.T.);
#566=FACE_BOUND('',#1419,.T.);
#567=FACE_BOUND('',#1420,.T.);
#568=FACE_BOUND('',#1424,.T.);
#569=FACE_BOUND('',#1425,.T.);
#720=PLANE('',#7003);
#721=PLANE('',#7004);
#722=PLANE('',#7005);
#723=PLANE('',#7006);
#724=PLANE('',#7007);
#725=PLANE('',#7008);
#726=PLANE('',#7009);
#727=PLANE('',#7010);
#728=PLANE('',#7011);
#729=PLANE('',#7012);
#967=FACE_OUTER_BOUND('',#1395,.T.);
#968=FACE_OUTER_BOUND('',#1396,.T.);
#969=FACE_OUTER_BOUND('',#1397,.T.);
#970=FACE_OUTER_BOUND('',#1398,.T.);
#971=FACE_OUTER_BOUND('',#1399,.T.);
#972=FACE_OUTER_BOUND('',#1400,.T.);
#973=FACE_OUTER_BOUND('',#1401,.T.);
#974=FACE_OUTER_BOUND('',#1402,.T.);
#975=FACE_OUTER_BOUND('',#1404,.T.);
#976=FACE_OUTER_BOUND('',#1406,.T.);
#977=FACE_OUTER_BOUND('',#1407,.T.);
#978=FACE_OUTER_BOUND('',#1408,.T.);
#979=FACE_OUTER_BOUND('',#1414,.T.);
#980=FACE_OUTER_BOUND('',#1415,.T.);
#981=FACE_OUTER_BOUND('',#1421,.T.);
#982=FACE_OUTER_BOUND('',#1422,.T.);
#983=FACE_OUTER_BOUND('',#1423,.T.);
#1395=EDGE_LOOP('',(#4642,#4643,#4644,#4645));
#1396=EDGE_LOOP('',(#4646,#4647,#4648,#4649));
#1397=EDGE_LOOP('',(#4650,#4651,#4652,#4653));
#1398=EDGE_LOOP('',(#4654,#4655,#4656,#4657));
#1399=EDGE_LOOP('',(#4658,#4659,#4660,#4661));
#1400=EDGE_LOOP('',(#4662,#4663,#4664,#4665));
#1401=EDGE_LOOP('',(#4666,#4667,#4668,#4669));
#1402=EDGE_LOOP('',(#4670,#4671,#4672,#4673));
#1403=EDGE_LOOP('',(#4674));
#1404=EDGE_LOOP('',(#4675,#4676,#4677,#4678));
#1405=EDGE_LOOP('',(#4679));
#1406=EDGE_LOOP('',(#4680,#4681,#4682,#4683));
#1407=EDGE_LOOP('',(#4684,#4685,#4686,#4687));
#1408=EDGE_LOOP('',(#4688,#4689,#4690,#4691,#4692,#4693,#4694,#4695));
#1409=EDGE_LOOP('',(#4696));
#1410=EDGE_LOOP('',(#4697));
#1411=EDGE_LOOP('',(#4698));
#1412=EDGE_LOOP('',(#4699));
#1413=EDGE_LOOP('',(#4700));
#1414=EDGE_LOOP('',(#4701,#4702,#4703,#4704));
#1415=EDGE_LOOP('',(#4705,#4706,#4707,#4708,#4709,#4710,#4711,#4712));
#1416=EDGE_LOOP('',(#4713));
#1417=EDGE_LOOP('',(#4714));
#1418=EDGE_LOOP('',(#4715));
#1419=EDGE_LOOP('',(#4716));
#1420=EDGE_LOOP('',(#4717));
#1421=EDGE_LOOP('',(#4718,#4719,#4720,#4721));
#1422=EDGE_LOOP('',(#4722,#4723,#4724,#4725));
#1423=EDGE_LOOP('',(#4726,#4727,#4728,#4729));
#1424=EDGE_LOOP('',(#4730));
#1425=EDGE_LOOP('',(#4731));
#1932=LINE('',#10074,#2371);
#1933=LINE('',#10080,#2372);
#1934=LINE('',#10086,#2373);
#1935=LINE('',#10092,#2374);
#1936=LINE('',#10098,#2375);
#1937=LINE('',#10104,#2376);
#1938=LINE('',#10110,#2377);
#1939=LINE('',#10115,#2378);
#1940=LINE('',#10117,#2379);
#1941=LINE('',#10119,#2380);
#1942=LINE('',#10120,#2381);
#1943=LINE('',#10124,#2382);
#1944=LINE('',#10126,#2383);
#1945=LINE('',#10128,#2384);
#1946=LINE('',#10129,#2385);
#1947=LINE('',#10132,#2386);
#1948=LINE('',#10134,#2387);
#1949=LINE('',#10135,#2388);
#1950=LINE('',#10138,#2389);
#1951=LINE('',#10140,#2390);
#1952=LINE('',#10141,#2391);
#1953=LINE('',#10144,#2392);
#1954=LINE('',#10146,#2393);
#1955=LINE('',#10147,#2394);
#1956=LINE('',#10148,#2395);
#1957=LINE('',#10151,#2396);
#1958=LINE('',#10152,#2397);
#1959=LINE('',#10155,#2398);
#1960=LINE('',#10156,#2399);
#1961=LINE('',#10157,#2400);
#1962=LINE('',#10159,#2401);
#2371=VECTOR('',#8030,0.225);
#2372=VECTOR('',#8037,0.225);
#2373=VECTOR('',#8044,0.165);
#2374=VECTOR('',#8051,0.165);
#2375=VECTOR('',#8058,0.165);
#2376=VECTOR('',#8065,0.165);
#2377=VECTOR('',#8072,1.6);
#2378=VECTOR('',#8077,1.);
#2379=VECTOR('',#8078,1.);
#2380=VECTOR('',#8079,1.);
#2381=VECTOR('',#8080,1.);
#2382=VECTOR('',#8083,1.);
#2383=VECTOR('',#8084,1.);
#2384=VECTOR('',#8085,1.);
#2385=VECTOR('',#8086,1.);
#2386=VECTOR('',#8089,1.);
#2387=VECTOR('',#8090,1.);
#2388=VECTOR('',#8091,1.);
#2389=VECTOR('',#8094,1.);
#2390=VECTOR('',#8095,1.);
#2391=VECTOR('',#8096,1.);
#2392=VECTOR('',#8099,1.);
#2393=VECTOR('',#8100,1.);
#2394=VECTOR('',#8101,1.);
#2395=VECTOR('',#8102,1.);
#2396=VECTOR('',#8105,1.);
#2397=VECTOR('',#8106,1.);
#2398=VECTOR('',#8109,1.);
#2399=VECTOR('',#8110,1.);
#2400=VECTOR('',#8111,1.);
#2401=VECTOR('',#8114,1.);
#2765=CIRCLE('',#6983,0.225);
#2766=CIRCLE('',#6984,0.225);
#2767=CIRCLE('',#6986,0.225);
#2768=CIRCLE('',#6987,0.225);
#2769=CIRCLE('',#6989,0.165);
#2770=CIRCLE('',#6990,0.165);
#2771=CIRCLE('',#6992,0.165);
#2772=CIRCLE('',#6993,0.165);
#2773=CIRCLE('',#6995,0.165);
#2774=CIRCLE('',#6996,0.165);
#2775=CIRCLE('',#6998,0.165);
#2776=CIRCLE('',#6999,0.165);
#2777=CIRCLE('',#7001,1.6);
#2778=CIRCLE('',#7002,1.6);
#3137=VERTEX_POINT('',#10071);
#3138=VERTEX_POINT('',#10073);
#3139=VERTEX_POINT('',#10077);
#3140=VERTEX_POINT('',#10079);
#3141=VERTEX_POINT('',#10083);
#3142=VERTEX_POINT('',#10085);
#3143=VERTEX_POINT('',#10089);
#3144=VERTEX_POINT('',#10091);
#3145=VERTEX_POINT('',#10095);
#3146=VERTEX_POINT('',#10097);
#3147=VERTEX_POINT('',#10101);
#3148=VERTEX_POINT('',#10103);
#3149=VERTEX_POINT('',#10107);
#3150=VERTEX_POINT('',#10109);
#3151=VERTEX_POINT('',#10113);
#3152=VERTEX_POINT('',#10114);
#3153=VERTEX_POINT('',#10116);
#3154=VERTEX_POINT('',#10118);
#3155=VERTEX_POINT('',#10122);
#3156=VERTEX_POINT('',#10123);
#3157=VERTEX_POINT('',#10125);
#3158=VERTEX_POINT('',#10127);
#3159=VERTEX_POINT('',#10131);
#3160=VERTEX_POINT('',#10133);
#3161=VERTEX_POINT('',#10137);
#3162=VERTEX_POINT('',#10139);
#3163=VERTEX_POINT('',#10143);
#3164=VERTEX_POINT('',#10145);
#3165=VERTEX_POINT('',#10150);
#3166=VERTEX_POINT('',#10154);
#3711=EDGE_CURVE('',#3137,#3137,#2765,.T.);
#3712=EDGE_CURVE('',#3137,#3138,#1932,.T.);
#3713=EDGE_CURVE('',#3138,#3138,#2766,.T.);
#3714=EDGE_CURVE('',#3139,#3139,#2767,.T.);
#3715=EDGE_CURVE('',#3139,#3140,#1933,.T.);
#3716=EDGE_CURVE('',#3140,#3140,#2768,.T.);
#3717=EDGE_CURVE('',#3141,#3141,#2769,.T.);
#3718=EDGE_CURVE('',#3141,#3142,#1934,.T.);
#3719=EDGE_CURVE('',#3142,#3142,#2770,.T.);
#3720=EDGE_CURVE('',#3143,#3143,#2771,.T.);
#3721=EDGE_CURVE('',#3143,#3144,#1935,.T.);
#3722=EDGE_CURVE('',#3144,#3144,#2772,.T.);
#3723=EDGE_CURVE('',#3145,#3145,#2773,.T.);
#3724=EDGE_CURVE('',#3145,#3146,#1936,.T.);
#3725=EDGE_CURVE('',#3146,#3146,#2774,.T.);
#3726=EDGE_CURVE('',#3147,#3147,#2775,.T.);
#3727=EDGE_CURVE('',#3147,#3148,#1937,.T.);
#3728=EDGE_CURVE('',#3148,#3148,#2776,.T.);
#3729=EDGE_CURVE('',#3149,#3149,#2777,.T.);
#3730=EDGE_CURVE('',#3149,#3150,#1938,.T.);
#3731=EDGE_CURVE('',#3150,#3150,#2778,.T.);
#3732=EDGE_CURVE('',#3151,#3152,#1939,.T.);
#3733=EDGE_CURVE('',#3153,#3151,#1940,.T.);
#3734=EDGE_CURVE('',#3153,#3154,#1941,.T.);
#3735=EDGE_CURVE('',#3152,#3154,#1942,.T.);
#3736=EDGE_CURVE('',#3155,#3156,#1943,.T.);
#3737=EDGE_CURVE('',#3157,#3155,#1944,.T.);
#3738=EDGE_CURVE('',#3158,#3157,#1945,.T.);
#3739=EDGE_CURVE('',#3156,#3158,#1946,.T.);
#3740=EDGE_CURVE('',#3158,#3159,#1947,.T.);
#3741=EDGE_CURVE('',#3160,#3157,#1948,.T.);
#3742=EDGE_CURVE('',#3159,#3160,#1949,.T.);
#3743=EDGE_CURVE('',#3161,#3153,#1950,.T.);
#3744=EDGE_CURVE('',#3161,#3162,#1951,.T.);
#3745=EDGE_CURVE('',#3154,#3162,#1952,.T.);
#3746=EDGE_CURVE('',#3151,#3163,#1953,.T.);
#3747=EDGE_CURVE('',#3164,#3163,#1954,.T.);
#3748=EDGE_CURVE('',#3156,#3164,#1955,.T.);
#3749=EDGE_CURVE('',#3159,#3161,#1956,.T.);
#3750=EDGE_CURVE('',#3152,#3165,#1957,.T.);
#3751=EDGE_CURVE('',#3163,#3165,#1958,.T.);
#3752=EDGE_CURVE('',#3155,#3166,#1959,.T.);
#3753=EDGE_CURVE('',#3165,#3166,#1960,.T.);
#3754=EDGE_CURVE('',#3162,#3160,#1961,.T.);
#3755=EDGE_CURVE('',#3166,#3164,#1962,.T.);
#4642=ORIENTED_EDGE('',*,*,#3711,.F.);
#4643=ORIENTED_EDGE('',*,*,#3712,.T.);
#4644=ORIENTED_EDGE('',*,*,#3713,.F.);
#4645=ORIENTED_EDGE('',*,*,#3712,.F.);
#4646=ORIENTED_EDGE('',*,*,#3714,.F.);
#4647=ORIENTED_EDGE('',*,*,#3715,.T.);
#4648=ORIENTED_EDGE('',*,*,#3716,.F.);
#4649=ORIENTED_EDGE('',*,*,#3715,.F.);
#4650=ORIENTED_EDGE('',*,*,#3717,.F.);
#4651=ORIENTED_EDGE('',*,*,#3718,.T.);
#4652=ORIENTED_EDGE('',*,*,#3719,.F.);
#4653=ORIENTED_EDGE('',*,*,#3718,.F.);
#4654=ORIENTED_EDGE('',*,*,#3720,.F.);
#4655=ORIENTED_EDGE('',*,*,#3721,.T.);
#4656=ORIENTED_EDGE('',*,*,#3722,.F.);
#4657=ORIENTED_EDGE('',*,*,#3721,.F.);
#4658=ORIENTED_EDGE('',*,*,#3723,.F.);
#4659=ORIENTED_EDGE('',*,*,#3724,.T.);
#4660=ORIENTED_EDGE('',*,*,#3725,.F.);
#4661=ORIENTED_EDGE('',*,*,#3724,.F.);
#4662=ORIENTED_EDGE('',*,*,#3726,.F.);
#4663=ORIENTED_EDGE('',*,*,#3727,.T.);
#4664=ORIENTED_EDGE('',*,*,#3728,.F.);
#4665=ORIENTED_EDGE('',*,*,#3727,.F.);
#4666=ORIENTED_EDGE('',*,*,#3729,.F.);
#4667=ORIENTED_EDGE('',*,*,#3730,.T.);
#4668=ORIENTED_EDGE('',*,*,#3731,.F.);
#4669=ORIENTED_EDGE('',*,*,#3730,.F.);
#4670=ORIENTED_EDGE('',*,*,#3732,.F.);
#4671=ORIENTED_EDGE('',*,*,#3733,.F.);
#4672=ORIENTED_EDGE('',*,*,#3734,.T.);
#4673=ORIENTED_EDGE('',*,*,#3735,.F.);
#4674=ORIENTED_EDGE('',*,*,#3716,.T.);
#4675=ORIENTED_EDGE('',*,*,#3736,.F.);
#4676=ORIENTED_EDGE('',*,*,#3737,.F.);
#4677=ORIENTED_EDGE('',*,*,#3738,.F.);
#4678=ORIENTED_EDGE('',*,*,#3739,.F.);
#4679=ORIENTED_EDGE('',*,*,#3713,.T.);
#4680=ORIENTED_EDGE('',*,*,#3740,.F.);
#4681=ORIENTED_EDGE('',*,*,#3738,.T.);
#4682=ORIENTED_EDGE('',*,*,#3741,.F.);
#4683=ORIENTED_EDGE('',*,*,#3742,.F.);
#4684=ORIENTED_EDGE('',*,*,#3743,.F.);
#4685=ORIENTED_EDGE('',*,*,#3744,.T.);
#4686=ORIENTED_EDGE('',*,*,#3745,.F.);
#4687=ORIENTED_EDGE('',*,*,#3734,.F.);
#4688=ORIENTED_EDGE('',*,*,#3746,.T.);
#4689=ORIENTED_EDGE('',*,*,#3747,.F.);
#4690=ORIENTED_EDGE('',*,*,#3748,.F.);
#4691=ORIENTED_EDGE('',*,*,#3739,.T.);
#4692=ORIENTED_EDGE('',*,*,#3740,.T.);
#4693=ORIENTED_EDGE('',*,*,#3749,.T.);
#4694=ORIENTED_EDGE('',*,*,#3743,.T.);
#4695=ORIENTED_EDGE('',*,*,#3733,.T.);
#4696=ORIENTED_EDGE('',*,*,#3729,.T.);
#4697=ORIENTED_EDGE('',*,*,#3726,.T.);
#4698=ORIENTED_EDGE('',*,*,#3723,.T.);
#4699=ORIENTED_EDGE('',*,*,#3720,.T.);
#4700=ORIENTED_EDGE('',*,*,#3717,.T.);
#4701=ORIENTED_EDGE('',*,*,#3732,.T.);
#4702=ORIENTED_EDGE('',*,*,#3750,.T.);
#4703=ORIENTED_EDGE('',*,*,#3751,.F.);
#4704=ORIENTED_EDGE('',*,*,#3746,.F.);
#4705=ORIENTED_EDGE('',*,*,#3752,.T.);
#4706=ORIENTED_EDGE('',*,*,#3753,.F.);
#4707=ORIENTED_EDGE('',*,*,#3750,.F.);
#4708=ORIENTED_EDGE('',*,*,#3735,.T.);
#4709=ORIENTED_EDGE('',*,*,#3745,.T.);
#4710=ORIENTED_EDGE('',*,*,#3754,.T.);
#4711=ORIENTED_EDGE('',*,*,#3741,.T.);
#4712=ORIENTED_EDGE('',*,*,#3737,.T.);
#4713=ORIENTED_EDGE('',*,*,#3731,.T.);
#4714=ORIENTED_EDGE('',*,*,#3728,.T.);
#4715=ORIENTED_EDGE('',*,*,#3725,.T.);
#4716=ORIENTED_EDGE('',*,*,#3722,.T.);
#4717=ORIENTED_EDGE('',*,*,#3719,.T.);
#4718=ORIENTED_EDGE('',*,*,#3736,.T.);
#4719=ORIENTED_EDGE('',*,*,#3748,.T.);
#4720=ORIENTED_EDGE('',*,*,#3755,.F.);
#4721=ORIENTED_EDGE('',*,*,#3752,.F.);
#4722=ORIENTED_EDGE('',*,*,#3755,.T.);
#4723=ORIENTED_EDGE('',*,*,#3747,.T.);
#4724=ORIENTED_EDGE('',*,*,#3751,.T.);
#4725=ORIENTED_EDGE('',*,*,#3753,.T.);
#4726=ORIENTED_EDGE('',*,*,#3754,.F.);
#4727=ORIENTED_EDGE('',*,*,#3744,.F.);
#4728=ORIENTED_EDGE('',*,*,#3749,.F.);
#4729=ORIENTED_EDGE('',*,*,#3742,.T.);
#4730=ORIENTED_EDGE('',*,*,#3711,.T.);
#4731=ORIENTED_EDGE('',*,*,#3714,.T.);
#5919=CYLINDRICAL_SURFACE('',#6982,0.225);
#5920=CYLINDRICAL_SURFACE('',#6985,0.225);
#5921=CYLINDRICAL_SURFACE('',#6988,0.165);
#5922=CYLINDRICAL_SURFACE('',#6991,0.165);
#5923=CYLINDRICAL_SURFACE('',#6994,0.165);
#5924=CYLINDRICAL_SURFACE('',#6997,0.165);
#5925=CYLINDRICAL_SURFACE('',#7000,1.6);
#6085=ADVANCED_FACE('',(#967),#5919,.F.);
#6086=ADVANCED_FACE('',(#968),#5920,.F.);
#6087=ADVANCED_FACE('',(#969),#5921,.F.);
#6088=ADVANCED_FACE('',(#970),#5922,.F.);
#6089=ADVANCED_FACE('',(#971),#5923,.F.);
#6090=ADVANCED_FACE('',(#972),#5924,.F.);
#6091=ADVANCED_FACE('',(#973),#5925,.F.);
#6092=ADVANCED_FACE('',(#974,#556),#720,.T.);
#6093=ADVANCED_FACE('',(#975,#557),#721,.T.);
#6094=ADVANCED_FACE('',(#976),#722,.T.);
#6095=ADVANCED_FACE('',(#977),#723,.T.);
#6096=ADVANCED_FACE('',(#978,#558,#559,#560,#561,#562),#724,.T.);
#6097=ADVANCED_FACE('',(#979),#725,.T.);
#6098=ADVANCED_FACE('',(#980,#563,#564,#565,#566,#567),#726,.T.);
#6099=ADVANCED_FACE('',(#981),#727,.T.);
#6100=ADVANCED_FACE('',(#982),#728,.T.);
#6101=ADVANCED_FACE('',(#983,#568,#569),#729,.F.);
#6404=CLOSED_SHELL('',(#6085,#6086,#6087,#6088,#6089,#6090,#6091,#6092,
#6093,#6094,#6095,#6096,#6097,#6098,#6099,#6100,#6101));
#6981=AXIS2_PLACEMENT_3D('',#10069,#8024,#8025);
#6982=AXIS2_PLACEMENT_3D('',#10070,#8026,#8027);
#6983=AXIS2_PLACEMENT_3D('',#10072,#8028,#8029);
#6984=AXIS2_PLACEMENT_3D('',#10075,#8031,#8032);
#6985=AXIS2_PLACEMENT_3D('',#10076,#8033,#8034);
#6986=AXIS2_PLACEMENT_3D('',#10078,#8035,#8036);
#6987=AXIS2_PLACEMENT_3D('',#10081,#8038,#8039);
#6988=AXIS2_PLACEMENT_3D('',#10082,#8040,#8041);
#6989=AXIS2_PLACEMENT_3D('',#10084,#8042,#8043);
#6990=AXIS2_PLACEMENT_3D('',#10087,#8045,#8046);
#6991=AXIS2_PLACEMENT_3D('',#10088,#8047,#8048);
#6992=AXIS2_PLACEMENT_3D('',#10090,#8049,#8050);
#6993=AXIS2_PLACEMENT_3D('',#10093,#8052,#8053);
#6994=AXIS2_PLACEMENT_3D('',#10094,#8054,#8055);
#6995=AXIS2_PLACEMENT_3D('',#10096,#8056,#8057);
#6996=AXIS2_PLACEMENT_3D('',#10099,#8059,#8060);
#6997=AXIS2_PLACEMENT_3D('',#10100,#8061,#8062);
#6998=AXIS2_PLACEMENT_3D('',#10102,#8063,#8064);
#6999=AXIS2_PLACEMENT_3D('',#10105,#8066,#8067);
#7000=AXIS2_PLACEMENT_3D('',#10106,#8068,#8069);
#7001=AXIS2_PLACEMENT_3D('',#10108,#8070,#8071);
#7002=AXIS2_PLACEMENT_3D('',#10111,#8073,#8074);
#7003=AXIS2_PLACEMENT_3D('',#10112,#8075,#8076);
#7004=AXIS2_PLACEMENT_3D('',#10121,#8081,#8082);
#7005=AXIS2_PLACEMENT_3D('',#10130,#8087,#8088);
#7006=AXIS2_PLACEMENT_3D('',#10136,#8092,#8093);
#7007=AXIS2_PLACEMENT_3D('',#10142,#8097,#8098);
#7008=AXIS2_PLACEMENT_3D('',#10149,#8103,#8104);
#7009=AXIS2_PLACEMENT_3D('',#10153,#8107,#8108);
#7010=AXIS2_PLACEMENT_3D('',#10158,#8112,#8113);
#7011=AXIS2_PLACEMENT_3D('',#10160,#8115,#8116);
#7012=AXIS2_PLACEMENT_3D('',#10161,#8117,#8118);
#8024=DIRECTION('axis',(0.,0.,1.));
#8025=DIRECTION('refdir',(1.,0.,0.));
#8026=DIRECTION('center_axis',(0.,0.,1.));
#8027=DIRECTION('ref_axis',(1.,0.,0.));
#8028=DIRECTION('center_axis',(0.,0.,1.));
#8029=DIRECTION('ref_axis',(1.,0.,0.));
#8030=DIRECTION('',(0.,0.,1.));
#8031=DIRECTION('center_axis',(0.,0.,-1.));
#8032=DIRECTION('ref_axis',(1.,0.,0.));
#8033=DIRECTION('center_axis',(0.,0.,1.));
#8034=DIRECTION('ref_axis',(1.,0.,0.));
#8035=DIRECTION('center_axis',(0.,0.,1.));
#8036=DIRECTION('ref_axis',(1.,0.,0.));
#8037=DIRECTION('',(0.,0.,1.));
#8038=DIRECTION('center_axis',(0.,0.,-1.));
#8039=DIRECTION('ref_axis',(1.,0.,0.));
#8040=DIRECTION('center_axis',(0.,1.,0.));
#8041=DIRECTION('ref_axis',(1.,0.,0.));
#8042=DIRECTION('center_axis',(0.,1.,0.));
#8043=DIRECTION('ref_axis',(1.,0.,0.));
#8044=DIRECTION('',(0.,1.,0.));
#8045=DIRECTION('center_axis',(0.,-1.,0.));
#8046=DIRECTION('ref_axis',(1.,0.,0.));
#8047=DIRECTION('center_axis',(0.,1.,0.));
#8048=DIRECTION('ref_axis',(1.,0.,0.));
#8049=DIRECTION('center_axis',(0.,1.,0.));
#8050=DIRECTION('ref_axis',(1.,0.,0.));
#8051=DIRECTION('',(0.,1.,0.));
#8052=DIRECTION('center_axis',(0.,-1.,0.));
#8053=DIRECTION('ref_axis',(1.,0.,0.));
#8054=DIRECTION('center_axis',(0.,1.,0.));
#8055=DIRECTION('ref_axis',(1.,0.,0.));
#8056=DIRECTION('center_axis',(0.,1.,0.));
#8057=DIRECTION('ref_axis',(1.,0.,0.));
#8058=DIRECTION('',(0.,1.,0.));
#8059=DIRECTION('center_axis',(0.,-1.,0.));
#8060=DIRECTION('ref_axis',(1.,0.,0.));
#8061=DIRECTION('center_axis',(0.,1.,0.));
#8062=DIRECTION('ref_axis',(1.,0.,0.));
#8063=DIRECTION('center_axis',(0.,1.,0.));
#8064=DIRECTION('ref_axis',(1.,0.,0.));
#8065=DIRECTION('',(0.,1.,0.));
#8066=DIRECTION('center_axis',(0.,-1.,0.));
#8067=DIRECTION('ref_axis',(1.,0.,0.));
#8068=DIRECTION('center_axis',(0.,1.,0.));
#8069=DIRECTION('ref_axis',(1.,0.,0.));
#8070=DIRECTION('center_axis',(0.,1.,0.));
#8071=DIRECTION('ref_axis',(1.,0.,0.));
#8072=DIRECTION('',(0.,1.,0.));
#8073=DIRECTION('center_axis',(0.,-1.,0.));
#8074=DIRECTION('ref_axis',(1.,0.,0.));
#8075=DIRECTION('center_axis',(0.,0.,1.));
#8076=DIRECTION('ref_axis',(1.,0.,0.));
#8077=DIRECTION('',(0.,1.,0.));
#8078=DIRECTION('',(-1.,0.,0.));
#8079=DIRECTION('',(0.,1.,0.));
#8080=DIRECTION('',(1.,0.,0.));
#8081=DIRECTION('center_axis',(0.,0.,1.));
#8082=DIRECTION('ref_axis',(1.,0.,0.));
#8083=DIRECTION('',(0.,-1.,0.));
#8084=DIRECTION('',(1.,0.,0.));
#8085=DIRECTION('',(0.,1.,0.));
#8086=DIRECTION('',(-1.,0.,0.));
#8087=DIRECTION('center_axis',(-1.,0.,0.));
#8088=DIRECTION('ref_axis',(0.,0.,1.));
#8089=DIRECTION('',(0.,0.,-1.));
#8090=DIRECTION('',(0.,0.,1.));
#8091=DIRECTION('',(0.,1.,0.));
#8092=DIRECTION('center_axis',(1.,0.,0.));
#8093=DIRECTION('ref_axis',(0.,0.,-1.));
#8094=DIRECTION('',(0.,0.,1.));
#8095=DIRECTION('',(0.,1.,0.));
#8096=DIRECTION('',(0.,0.,-1.));
#8097=DIRECTION('center_axis',(0.,-1.,0.));
#8098=DIRECTION('ref_axis',(1.,0.,0.));
#8099=DIRECTION('',(0.,0.,1.));
#8100=DIRECTION('',(1.,0.,0.));
#8101=DIRECTION('',(0.,0.,1.));
#8102=DIRECTION('',(1.,0.,0.));
#8103=DIRECTION('center_axis',(1.,0.,0.));
#8104=DIRECTION('ref_axis',(0.,1.,0.));
#8105=DIRECTION('',(0.,0.,1.));
#8106=DIRECTION('',(0.,1.,0.));
#8107=DIRECTION('center_axis',(0.,1.,0.));
#8108=DIRECTION('ref_axis',(-1.,0.,0.));
#8109=DIRECTION('',(0.,0.,1.));
#8110=DIRECTION('',(-1.,0.,0.));
#8111=DIRECTION('',(-1.,0.,0.));
#8112=DIRECTION('center_axis',(-1.,0.,0.));
#8113=DIRECTION('ref_axis',(0.,-1.,0.));
#8114=DIRECTION('',(0.,-1.,0.));
#8115=DIRECTION('center_axis',(0.,0.,1.));
#8116=DIRECTION('ref_axis',(1.,0.,0.));
#8117=DIRECTION('center_axis',(0.,0.,1.));
#8118=DIRECTION('ref_axis',(1.,0.,0.));
#10069=CARTESIAN_POINT('',(0.,0.,0.));
#10070=CARTESIAN_POINT('Origin',(-3.,2.5,0.9));
#10071=CARTESIAN_POINT('',(-3.225,2.5,1.));
#10072=CARTESIAN_POINT('Origin',(-3.,2.5,1.));
#10073=CARTESIAN_POINT('',(-3.225,2.5,1.8));
#10074=CARTESIAN_POINT('',(-3.225,2.5,0.9));
#10075=CARTESIAN_POINT('Origin',(-3.,2.5,1.8));
#10076=CARTESIAN_POINT('Origin',(3.,2.5,0.9));
#10077=CARTESIAN_POINT('',(2.775,2.5,1.));
#10078=CARTESIAN_POINT('Origin',(3.,2.5,1.));
#10079=CARTESIAN_POINT('',(2.775,2.5,1.8));
#10080=CARTESIAN_POINT('',(2.775,2.5,0.9));
#10081=CARTESIAN_POINT('Origin',(3.,2.5,1.8));
#10082=CARTESIAN_POINT('Origin',(-1.4142135623731,1.6,2.58578643762691));
#10083=CARTESIAN_POINT('',(-1.5792135623731,1.7,2.58578643762691));
#10084=CARTESIAN_POINT('Origin',(-1.4142135623731,1.7,2.58578643762691));
#10085=CARTESIAN_POINT('',(-1.5792135623731,3.3,2.58578643762691));
#10086=CARTESIAN_POINT('',(-1.5792135623731,1.6,2.58578643762691));
#10087=CARTESIAN_POINT('Origin',(-1.4142135623731,3.3,2.58578643762691));
#10088=CARTESIAN_POINT('Origin',(-1.41421356237309,1.6,5.41421356237309));
#10089=CARTESIAN_POINT('',(-1.57921356237309,1.7,5.41421356237309));
#10090=CARTESIAN_POINT('Origin',(-1.41421356237309,1.7,5.41421356237309));
#10091=CARTESIAN_POINT('',(-1.57921356237309,3.3,5.41421356237309));
#10092=CARTESIAN_POINT('',(-1.57921356237309,1.6,5.41421356237309));
#10093=CARTESIAN_POINT('Origin',(-1.41421356237309,3.3,5.41421356237309));
#10094=CARTESIAN_POINT('Origin',(1.4142135623731,1.6,5.41421356237309));
#10095=CARTESIAN_POINT('',(1.2492135623731,1.7,5.41421356237309));
#10096=CARTESIAN_POINT('Origin',(1.4142135623731,1.7,5.41421356237309));
#10097=CARTESIAN_POINT('',(1.2492135623731,3.3,5.41421356237309));
#10098=CARTESIAN_POINT('',(1.2492135623731,1.6,5.41421356237309));
#10099=CARTESIAN_POINT('Origin',(1.4142135623731,3.3,5.41421356237309));
#10100=CARTESIAN_POINT('Origin',(1.41421356237309,1.6,2.5857864376269));
#10101=CARTESIAN_POINT('',(1.24921356237309,1.7,2.5857864376269));
#10102=CARTESIAN_POINT('Origin',(1.41421356237309,1.7,2.5857864376269));
#10103=CARTESIAN_POINT('',(1.24921356237309,3.3,2.5857864376269));
#10104=CARTESIAN_POINT('',(1.24921356237309,1.6,2.5857864376269));
#10105=CARTESIAN_POINT('Origin',(1.41421356237309,3.3,2.5857864376269));
#10106=CARTESIAN_POINT('Origin',(0.,1.6,4.));
#10107=CARTESIAN_POINT('',(-1.6,1.7,4.));
#10108=CARTESIAN_POINT('Origin',(0.,1.7,4.));
#10109=CARTESIAN_POINT('',(-1.6,3.3,4.));
#10110=CARTESIAN_POINT('',(-1.6,1.6,4.));
#10111=CARTESIAN_POINT('Origin',(0.,3.3,4.));
#10112=CARTESIAN_POINT('Origin',(-3.6,1.7,1.8));
#10113=CARTESIAN_POINT('',(2.4,1.7,1.8));
#10114=CARTESIAN_POINT('',(2.4,3.3,1.8));
#10115=CARTESIAN_POINT('',(2.4,1.7,1.8));
#10116=CARTESIAN_POINT('',(3.6,1.7,1.8));
#10117=CARTESIAN_POINT('',(3.6,1.7,1.8));
#10118=CARTESIAN_POINT('',(3.6,3.3,1.8));
#10119=CARTESIAN_POINT('',(3.6,1.7,1.8));
#10120=CARTESIAN_POINT('',(3.6,3.3,1.8));
#10121=CARTESIAN_POINT('Origin',(-3.6,1.7,1.8));
#10122=CARTESIAN_POINT('',(-2.4,3.3,1.8));
#10123=CARTESIAN_POINT('',(-2.4,1.7,1.8));
#10124=CARTESIAN_POINT('',(-2.4,2.5,1.8));
#10125=CARTESIAN_POINT('',(-3.6,3.3,1.8));
#10126=CARTESIAN_POINT('',(3.6,3.3,1.8));
#10127=CARTESIAN_POINT('',(-3.6,1.7,1.8));
#10128=CARTESIAN_POINT('',(-3.6,1.7,1.8));
#10129=CARTESIAN_POINT('',(3.6,1.7,1.8));
#10130=CARTESIAN_POINT('Origin',(-3.6,1.7,1.));
#10131=CARTESIAN_POINT('',(-3.6,1.7,1.));
#10132=CARTESIAN_POINT('',(-3.6,1.7,1.8));
#10133=CARTESIAN_POINT('',(-3.6,3.3,1.));
#10134=CARTESIAN_POINT('',(-3.6,3.3,1.8));
#10135=CARTESIAN_POINT('',(-3.6,1.7,1.));
#10136=CARTESIAN_POINT('Origin',(3.6,1.7,1.8));
#10137=CARTESIAN_POINT('',(3.6,1.7,1.));
#10138=CARTESIAN_POINT('',(3.6,1.7,1.));
#10139=CARTESIAN_POINT('',(3.6,3.3,1.));
#10140=CARTESIAN_POINT('',(3.6,1.7,1.));
#10141=CARTESIAN_POINT('',(3.6,3.3,1.));
#10142=CARTESIAN_POINT('Origin',(-2.4,1.7,1.));
#10143=CARTESIAN_POINT('',(2.4,1.7,6.5));
#10144=CARTESIAN_POINT('',(2.4,1.7,1.));
#10145=CARTESIAN_POINT('',(-2.4,1.7,6.5));
#10146=CARTESIAN_POINT('',(-2.4,1.7,6.5));
#10147=CARTESIAN_POINT('',(-2.4,1.7,1.));
#10148=CARTESIAN_POINT('',(-3.6,1.7,1.));
#10149=CARTESIAN_POINT('Origin',(2.4,1.7,1.));
#10150=CARTESIAN_POINT('',(2.4,3.3,6.5));
#10151=CARTESIAN_POINT('',(2.4,3.3,1.));
#10152=CARTESIAN_POINT('',(2.4,1.7,6.5));
#10153=CARTESIAN_POINT('Origin',(2.4,3.3,1.));
#10154=CARTESIAN_POINT('',(-2.4,3.3,6.5));
#10155=CARTESIAN_POINT('',(-2.4,3.3,1.));
#10156=CARTESIAN_POINT('',(2.4,3.3,6.5));
#10157=CARTESIAN_POINT('',(-3.6,3.3,1.));
#10158=CARTESIAN_POINT('Origin',(-2.4,3.3,1.));
#10159=CARTESIAN_POINT('',(-2.4,3.3,6.5));
#10160=CARTESIAN_POINT('Origin',(0.,2.5,6.5));
#10161=CARTESIAN_POINT('Origin',(0.,2.5,1.));
#13198=UNCERTAINTY_MEASURE_WITH_UNIT(LENGTH_MEASURE(0.001),#13278,
'DISTANCE_ACCURACY_VALUE',
'Maximum model space distance between geometric entities at asserted c
onnectivities');
#13233=UNCERTAINTY_MEASURE_WITH_UNIT(LENGTH_MEASURE(0.001),#13278,
'DISTANCE_ACCURACY_VALUE',
'Maximum model space distance between geometric entities at asserted c
onnectivities');
#13242=(
GEOMETRIC_REPRESENTATION_CONTEXT(3)
GLOBAL_UNCERTAINTY_ASSIGNED_CONTEXT((#13198))
GLOBAL_UNIT_ASSIGNED_CONTEXT((#13278,#13280,#13281))
REPRESENTATION_CONTEXT('','3D')
);
#13277=(
GEOMETRIC_REPRESENTATION_CONTEXT(3)
GLOBAL_UNCERTAINTY_ASSIGNED_CONTEXT((#13233))
GLOBAL_UNIT_ASSIGNED_CONTEXT((#13278,#13280,#13281))
REPRESENTATION_CONTEXT('','3D')
);
#13278=(
LENGTH_UNIT()
NAMED_UNIT(*)
SI_UNIT(.CENTI.,.METRE.)
);
#13280=(
NAMED_UNIT(*)
PLANE_ANGLE_UNIT()
SI_UNIT($,.RADIAN.)
);
#13281=(
NAMED_UNIT(*)
SI_UNIT($,.STERADIAN.)
SOLID_ANGLE_UNIT()
);
#13290=SHAPE_DEFINITION_REPRESENTATION(#13333,#13447);
#13333=PRODUCT_DEFINITION_SHAPE('',$,#13491);
#13447=SHAPE_REPRESENTATION('',(#6981),#13242);
#13482=PRODUCT_DEFINITION_CONTEXT('part definition',#13613,'design');
#13491=PRODUCT_DEFINITION('Camshaft bearing post (1)',
'Camshaft bearing post (1)',#13534,#13482);
#13534=PRODUCT_DEFINITION_FORMATION('',$,#13623);
#13613=APPLICATION_CONTEXT(
'Core Data for Automotive Mechanical Design Process');
#13614=PRODUCT_CONTEXT('part definition',#13613,'mechanical');
#13623=PRODUCT('Camshaft bearing post (1)','Camshaft bearing post (1)',
'Camshaft bearing post (1)',(#13614));
#13714=COLOUR_RGB('Grey',0.48,0.52,0.57);
#13715=FILL_AREA_STYLE_COLOUR('',#13714);
#13716=FILL_AREA_STYLE('',(#13715));
#13717=SURFACE_STYLE_FILL_AREA(#13716);
#13718=SURFACE_SIDE_STYLE('',(#13717));
#13719=SURFACE_STYLE_USAGE(.BOTH.,#13718);
#13720=PRESENTATION_STYLE_ASSIGNMENT((#13719));
ENDSEC;
END-ISO-10303-21;
